ISO-10303-21;
HEADER;
FILE_DESCRIPTION (('STEP AP214'),
    '1' );
FILE_NAME ('V-Link.step',
    '2026-10-28T16:39:03',
    ( '' ),
    ( '' ),
    'SwSTEP 2.0',
    'SolidWorks 2024',
    '' );
FILE_SCHEMA (( 'AUTOMOTIVE_DESIGN' ));
ENDSEC;

DATA;
#7=LINE ( 'NONE', #3105, #4260 ) ;
#43=EDGE_CURVE ( 'NONE', #2392, #5200, #812, .T. ) ;
#57=AXIS2_PLACEMENT_3D ( 'NONE', #6318, #3273, #5723 ) ;
#82=FACE_OUTER_BOUND ( 'NONE', #3199, .T. ) ;
#98=CYLINDRICAL_SURFACE ( 'NONE', #6896, 12.50000000000001066 ) ;
#106=VECTOR ( 'NONE', #6998, 1000.000000000000000 ) ;
#120=ORIENTED_EDGE ( 'NONE', *, *, #43, .F. ) ;
#139=CYLINDRICAL_SURFACE ( 'NONE', #3161, 24.99999999999999289 ) ;
#151=DIRECTION ( 'NONE',  ( 0.000000000000000000, 0.000000000000000000, 1.000000000000000000 ) ) ;
#154=CARTESIAN_POINT ( 'NONE',  ( 138.5360707071662887, -22.21662272193747256, 0.000000000000000000 ) ) ;
#162=CARTESIAN_POINT ( 'NONE',  ( -25.00000000000000711, 0.000000000000000000, 0.000000000000000000 ) ) ;
#197=ORIENTED_EDGE ( 'NONE', *, *, #6177, .T. ) ;
#200=DIRECTION ( 'NONE',  ( -0.000000000000000000, -0.000000000000000000, -1.000000000000000000 ) ) ;
#235=CIRCLE ( 'NONE', #1138, 12.50000000000000000 ) ;
#296=ORIENTED_EDGE ( 'NONE', *, *, #1888, .F. ) ;
#313=EDGE_LOOP ( 'NONE', ( #5764, #1754 ) ) ;
#368=LINE ( 'NONE', #970, #2555 ) ;
#392=DIRECTION ( 'NONE',  ( 1.000000000000000000, 0.000000000000000000, 0.000000000000000000 ) ) ;
#399=EDGE_LOOP ( 'NONE', ( #7198, #2677, #721, #3048 ) ) ;
#426=ORIENTED_EDGE ( 'NONE', *, *, #43, .T. ) ;
#542=DIRECTION ( 'NONE',  ( -1.000000000000000000, 0.000000000000000000, 0.000000000000000000 ) ) ;
#551=( NAMED_UNIT ( * ) PLANE_ANGLE_UNIT ( ) SI_UNIT ( $, .RADIAN. ) );
#585=CARTESIAN_POINT ( 'NONE',  ( 150.0000000000000000, 1.836970198721029747E-14, 0.000000000000000000 ) ) ;
#587=CIRCLE ( 'NONE', #3639, 12.50000000000001066 ) ;
#673=FACE_OUTER_BOUND ( 'NONE', #4002, .T. ) ;
#685=FACE_OUTER_BOUND ( 'NONE', #1976, .T. ) ;
#693=DIRECTION ( 'NONE',  ( -0.000000000000000000, -0.000000000000000000, -1.000000000000000000 ) ) ;
#702=VECTOR ( 'NONE', #6970, 1000.000000000000000 ) ;
#721=ORIENTED_EDGE ( 'NONE', *, *, #3608, .F. ) ;
#723=DIRECTION ( 'NONE',  ( 1.000000000000000000, 0.000000000000000000, 0.000000000000000000 ) ) ;
#741=DIRECTION ( 'NONE',  ( -1.000000000000000000, 0.000000000000000000, 0.000000000000000000 ) ) ;
#745=ORIENTED_EDGE ( 'NONE', *, *, #6400, .T. ) ;
#759=ORIENTED_EDGE ( 'NONE', *, *, #6177, .F. ) ;
#796=DIRECTION ( 'NONE',  ( 0.000000000000000000, 0.000000000000000000, 1.000000000000000000 ) ) ;
#812=CIRCLE ( 'NONE', #4650, 25.00000000000000711 ) ;
#829=DIRECTION ( 'NONE',  ( -1.000000000000000000, 0.000000000000000000, 0.000000000000000000 ) ) ;
#868=CARTESIAN_POINT ( 'NONE',  ( -8.959197987552832032, 23.33951095074251114, 25.00000000000000000 ) ) ;
#886=VERTEX_POINT ( 'NONE', #2697 ) ;
#892=DIRECTION ( 'NONE',  ( 0.8886649088774987160, 0.4585571717133501424, -0.000000000000000000 ) ) ;
#895=CARTESIAN_POINT ( 'NONE',  ( 137.4999999999999716, 1.836970198721029747E-14, 0.000000000000000000 ) ) ;
#911=EDGE_CURVE ( 'NONE', #886, #5200, #2738, .T. ) ;
#944=VECTOR ( 'NONE', #4047, 1000.000000000000000 ) ;
#949=SHAPE_REPRESENTATION ( 'V-Link', ( #5785 ), #2447 ) ;
#957=VERTEX_POINT ( 'NONE', #5131 ) ;
#970=CARTESIAN_POINT ( 'NONE',  ( 75.00000000000000000, 10.56842436860067735, 25.00000000000000000 ) ) ;
#986=ORIENTED_EDGE ( 'NONE', *, *, #3424, .T. ) ;
#1049=CARTESIAN_POINT ( 'NONE',  ( 0.000000000000000000, 0.000000000000000000, 25.00000000000000000 ) ) ;
#1061=EDGE_CURVE ( 'NONE', #3356, #886, #6981, .T. ) ;
#1092=CARTESIAN_POINT ( 'NONE',  ( 75.00000000000000000, 55.56842436860067380, 25.00000000000000000 ) ) ;
#1096=EDGE_LOOP ( 'NONE', ( #6058, #4187, #3905, #4902 ) ) ;
#1098=AXIS2_PLACEMENT_3D ( 'NONE', #5651, #2596, #829 ) ;
#1138=AXIS2_PLACEMENT_3D ( 'NONE', #4103, #7761, #6634 ) ;
#1148=CARTESIAN_POINT ( 'NONE',  ( -12.50000000000000000, 0.000000000000000000, 0.000000000000000000 ) ) ;
#1149=CARTESIAN_POINT ( 'NONE',  ( 0.000000000000000000, 0.000000000000000000, 25.00000000000000000 ) ) ;
#1157=ADVANCED_FACE ( 'NONE', ( #82 ), #6147, .T. ) ;
#1210=CARTESIAN_POINT ( 'NONE',  ( 75.00000000000000000, 55.56842436860067380, 25.00000000000000000 ) ) ;
#1223=ORIENTED_EDGE ( 'NONE', *, *, #1408, .F. ) ;
#1227=DIRECTION ( 'NONE',  ( -1.000000000000000000, 0.000000000000000000, 0.000000000000000000 ) ) ;
#1232=CARTESIAN_POINT ( 'NONE',  ( 158.9591979875528409, 23.33951095074252891, 25.00000000000000000 ) ) ;
#1263=EDGE_CURVE ( 'NONE', #2186, #7887, #7, .T. ) ;
#1328=PRODUCT_CONTEXT ( 'NONE', #2748, 'mechanical' ) ;
#1358=STYLED_ITEM('',(#7948),#4135);
#1363=CARTESIAN_POINT ( 'NONE',  ( 75.00000000000000000, 10.56842436860067735, 25.00000000000000000 ) ) ;
#1381=CARTESIAN_POINT ( 'NONE',  ( -8.959197987552832032, 23.33951095074251114, 25.00000000000000000 ) ) ;
#1408=EDGE_CURVE ( 'NONE', #4601, #6800, #2511, .T. ) ;
#1416=ORIENTED_EDGE ( 'NONE', *, *, #5665, .T. ) ;
#1417=FACE_OUTER_BOUND ( 'NONE', #4360, .T. ) ;
#1430=ORIENTED_EDGE ( 'NONE', *, *, #6604, .T. ) ;
#1434=ADVANCED_BREP_SHAPE_REPRESENTATION ( '', ( #4135, #5785 ), #2447 ) ;
#1478=CIRCLE ( 'NONE', #6101, 12.50000000000001066 ) ;
#1484=ORIENTED_EDGE ( 'NONE', *, *, #6553, .T. ) ;
#1503=ORIENTED_EDGE ( 'NONE', *, *, #4873, .T. ) ;
#1521=CARTESIAN_POINT ( 'NONE',  ( 0.000000000000000000, 0.000000000000000000, 0.000000000000000000 ) ) ;
#1527=DIRECTION ( 'NONE',  ( -1.000000000000000000, 0.000000000000000000, 0.000000000000000000 ) ) ;
#1537=CARTESIAN_POINT ( 'NONE',  ( 158.9591979875528409, 23.33951095074252891, 25.00000000000000000 ) ) ;
#1554=VERTEX_POINT ( 'NONE', #4348 ) ;
#1577=AXIS2_PLACEMENT_3D ( 'NONE', #5427, #7870, #4821 ) ;
#1589=EDGE_CURVE ( 'NONE', #7759, #7887, #6804, .T. ) ;
#1617=DIRECTION ( 'NONE',  ( 0.3583679195021131081, -0.9335804380297002547, 0.000000000000000000 ) ) ;
#1631=ORIENTED_EDGE ( 'NONE', *, *, #911, .F. ) ;
#1638=DIRECTION ( 'NONE',  ( 1.000000000000000000, 0.000000000000000000, 0.000000000000000000 ) ) ;
#1640=VECTOR ( 'NONE', #7186, 1000.000000000000000 ) ;
#1654=EDGE_CURVE ( 'NONE', #7759, #3356, #7610, .T. ) ;
#1683=CARTESIAN_POINT ( 'NONE',  ( 150.0000000000000000, 1.836970198721029747E-14, 0.000000000000000000 ) ) ;
#1742=ORIENTED_EDGE ( 'NONE', *, *, #4873, .F. ) ;
#1754=ORIENTED_EDGE ( 'NONE', *, *, #1890, .T. ) ;
#1843=DIRECTION ( 'NONE',  ( -0.000000000000000000, -0.000000000000000000, -1.000000000000000000 ) ) ;
#1888=EDGE_CURVE ( 'NONE', #4997, #3351, #1961, .T. ) ;
#1890=EDGE_CURVE ( 'NONE', #1554, #4302, #587, .T. ) ;
#1911=EDGE_CURVE ( 'NONE', #957, #4302, #6950, .T. ) ;
#1946=ORIENTED_EDGE ( 'NONE', *, *, #5665, .F. ) ;
#1947=DIRECTION ( 'NONE',  ( -1.000000000000000000, 0.000000000000000000, 0.000000000000000000 ) ) ;
#1961=CIRCLE ( 'NONE', #1577, 24.99999999999999289 ) ;
#1971=VECTOR ( 'NONE', #2615, 1000.000000000000000 ) ;
#1976=EDGE_LOOP ( 'NONE', ( #2884, #3176, #3092, #745 ) ) ;
#1992=CIRCLE ( 'NONE', #3153, 12.50000000000000000 ) ;
#2052=CARTESIAN_POINT ( 'NONE',  ( 137.4999999999999716, 1.836970198721029747E-14, 25.00000000000000000 ) ) ;
#2068=DIRECTION ( 'NONE',  ( -0.9335804380297002547, -0.3583679195021130526, -0.000000000000000000 ) ) ;
#2096=ORIENTED_EDGE ( 'NONE', *, *, #6207, .T. ) ;
#2097=PLANE ( 'NONE',  #7513 ) ;
#2103=ORIENTED_EDGE ( 'NONE', *, *, #5241, .F. ) ;
#2139=CARTESIAN_POINT ( 'NONE',  ( -8.959197987552832032, 23.33951095074251114, 25.00000000000000000 ) ) ;
#2151=CARTESIAN_POINT ( 'NONE',  ( 75.00000000000000000, 10.56842436860067735, 25.00000000000000000 ) ) ;
#2165=DIRECTION ( 'NONE',  ( -0.000000000000000000, -0.000000000000000000, -1.000000000000000000 ) ) ;
#2186=VERTEX_POINT ( 'NONE', #6107 ) ;
#2198=PRODUCT ( 'V-Link', 'V-Link', '', ( #1328 ) ) ;
#2201=LINE ( 'NONE', #7016, #7294 ) ;
#2208=LINE ( 'NONE', #4005, #1640 ) ;
#2215=DIRECTION ( 'NONE',  ( -0.000000000000000000, -0.000000000000000000, -1.000000000000000000 ) ) ;
#2280=PLANE ( 'NONE',  #2383 ) ;
#2285=LINE ( 'NONE', #5971, #7373 ) ;
#2330=ORIENTED_EDGE ( 'NONE', *, *, #6604, .F. ) ;
#2351=DIRECTION ( 'NONE',  ( 1.000000000000000000, 0.000000000000000000, 0.000000000000000000 ) ) ;
#2373=LINE ( 'NONE', #7110, #6781 ) ;
#2383=AXIS2_PLACEMENT_3D ( 'NONE', #2151, #4594, #2716 ) ;
#2392=VERTEX_POINT ( 'NONE', #162 ) ;
#2424=DIRECTION ( 'NONE',  ( 0.000000000000000000, 0.000000000000000000, 1.000000000000000000 ) ) ;
#2426=AXIS2_PLACEMENT_3D ( 'NONE', #4366, #6146, #7429 ) ;
#2432=CARTESIAN_POINT ( 'NONE',  ( 0.000000000000000000, 0.000000000000000000, 25.00000000000000000 ) ) ;
#2443=DIRECTION ( 'NONE',  ( 1.000000000000000000, 0.000000000000000000, -0.000000000000000000 ) ) ;
#2447=( GEOMETRIC_REPRESENTATION_CONTEXT ( 3 ) GLOBAL_UNCERTAINTY_ASSIGNED_CONTEXT ( ( #2473 ) ) GLOBAL_UNIT_ASSIGNED_CONTEXT ( ( #2506, #3678, #5515 ) ) REPRESENTATION_CONTEXT ( 'NONE', 'WORKASPACE' ) );
#2459=ADVANCED_FACE ( 'NONE', ( #685 ), #5704, .T. ) ;
#2473=UNCERTAINTY_MEASURE_WITH_UNIT (LENGTH_MEASURE( 1.000000000000000082E-05 ), #2506, 'distance_accuracy_value', 'NONE');
#2504=ADVANCED_FACE ( 'NONE', ( #7100 ), #2730, .F. ) ;
#2506=( LENGTH_UNIT ( ) NAMED_UNIT ( * ) SI_UNIT ( .MILLI., .METRE. ) );
#2511=LINE ( 'NONE', #4951, #944 ) ;
#2518=LINE ( 'NONE', #868, #7125 ) ;
#2536=VECTOR ( 'NONE', #2165, 1000.000000000000000 ) ;
#2550=CARTESIAN_POINT ( 'NONE',  ( 150.0000000000000000, 1.836970198721029747E-14, 25.00000000000000000 ) ) ;
#2555=VECTOR ( 'NONE', #6582, 1000.000000000000227 ) ;
#2590=CARTESIAN_POINT ( 'NONE',  ( -25.00000000000000711, 0.000000000000000000, 25.00000000000000000 ) ) ;
#2596=DIRECTION ( 'NONE',  ( -0.000000000000000000, -0.000000000000000000, -1.000000000000000000 ) ) ;
#2615=DIRECTION ( 'NONE',  ( -0.000000000000000000, -0.000000000000000000, -1.000000000000000000 ) ) ;
#2633=ORIENTED_EDGE ( 'NONE', *, *, #3755, .F. ) ;
#2638=CARTESIAN_POINT ( 'NONE',  ( 150.0000000000000000, 1.836970198721029747E-14, 0.000000000000000000 ) ) ;
#2654=AXIS2_PLACEMENT_3D ( 'NONE', #6633, #2424, #542 ) ;
#2673=EDGE_CURVE ( 'NONE', #2860, #4784, #4788, .T. ) ;
#2677=ORIENTED_EDGE ( 'NONE', *, *, #1408, .T. ) ;
#2688=ORIENTED_EDGE ( 'NONE', *, *, #3226, .F. ) ;
#2694=ORIENTED_EDGE ( 'NONE', *, *, #1911, .F. ) ;
#2697=CARTESIAN_POINT ( 'NONE',  ( 11.46392929283375928, -22.21662272193747256, 25.00000000000000000 ) ) ;
#2710=PRODUCT_DEFINITION_SHAPE ( 'NONE', 'NONE',  #4720 ) ;
#2711=PLANE ( 'NONE',  #6351 ) ;
#2712=UNCERTAINTY_MEASURE_WITH_UNIT (LENGTH_MEASURE( 1.000000000000000082E-05 ), #7252, 'distance_accuracy_value', 'NONE');
#2716=DIRECTION ( 'NONE',  ( -0.8886649088774988270, -0.4585571717133501424, 0.000000000000000000 ) ) ;
#2730=CYLINDRICAL_SURFACE ( 'NONE', #3650, 12.50000000000001066 ) ;
#2738=LINE ( 'NONE', #7551, #1971 ) ;
#2748=APPLICATION_CONTEXT ( 'automotive_design' ) ;
#2777=CARTESIAN_POINT ( 'NONE',  ( 12.50000000000000000, 1.530808498934191521E-15, 25.00000000000000000 ) ) ;
#2800=ORIENTED_EDGE ( 'NONE', *, *, #1263, .T. ) ;
#2820=DIRECTION ( 'NONE',  ( 0.8886649088774989380, -0.4585571717133497538, 0.000000000000000000 ) ) ;
#2821=DIRECTION ( 'NONE',  ( 0.000000000000000000, 0.000000000000000000, 1.000000000000000000 ) ) ;
#2860=VERTEX_POINT ( 'NONE', #154 ) ;
#2884=ORIENTED_EDGE ( 'NONE', *, *, #3057, .F. ) ;
#2903=DIRECTION ( 'NONE',  ( 1.000000000000000000, 0.000000000000000000, 0.000000000000000000 ) ) ;
#2943=EDGE_LOOP ( 'NONE', ( #4086, #1430, #5952, #2694 ) ) ;
#2946=DIRECTION ( 'NONE',  ( 0.000000000000000000, 0.000000000000000000, 1.000000000000000000 ) ) ;
#2986=DIRECTION ( 'NONE',  ( -0.000000000000000000, -0.000000000000000000, -1.000000000000000000 ) ) ;
#3000=FACE_BOUND ( 'NONE', #3120, .T. ) ;
#3017=ORIENTED_EDGE ( 'NONE', *, *, #5069, .F. ) ;
#3028=VECTOR ( 'NONE', #892, 1000.000000000000227 ) ;
#3035=DIRECTION ( 'NONE',  ( 0.000000000000000000, 0.000000000000000000, 1.000000000000000000 ) ) ;
#3048=ORIENTED_EDGE ( 'NONE', *, *, #6253, .F. ) ;
#3049=VECTOR ( 'NONE', #7428, 1000.000000000000227 ) ;
#3052=CARTESIAN_POINT ( 'NONE',  ( 0.000000000000000000, 0.000000000000000000, 0.000000000000000000 ) ) ;
#3057=EDGE_CURVE ( 'NONE', #3356, #2392, #4633, .T. ) ;
#3063=CARTESIAN_POINT ( 'NONE',  ( 138.5360707071662887, -22.21662272193747256, 25.00000000000000000 ) ) ;
#3092=ORIENTED_EDGE ( 'NONE', *, *, #1589, .T. ) ;
#3105=CARTESIAN_POINT ( 'NONE',  ( -8.959197987552832032, 23.33951095074251114, 0.000000000000000000 ) ) ;
#3120=EDGE_LOOP ( 'NONE', ( #7177, #5313 ) ) ;
#3140=DIRECTION ( 'NONE',  ( -0.9335804380297002547, -0.3583679195021130526, -0.000000000000000000 ) ) ;
#3153=AXIS2_PLACEMENT_3D ( 'NONE', #1521, #3965, #1638 ) ;
#3156=FACE_OUTER_BOUND ( 'NONE', #4656, .T. ) ;
#3158=DIRECTION ( 'NONE',  ( -0.000000000000000000, -0.000000000000000000, -1.000000000000000000 ) ) ;
#3161=AXIS2_PLACEMENT_3D ( 'NONE', #4947, #7405, #6836 ) ;
#3164=ORIENTED_EDGE ( 'NONE', *, *, #6302, .T. ) ;
#3176=ORIENTED_EDGE ( 'NONE', *, *, #1654, .F. ) ;
#3199=EDGE_LOOP ( 'NONE', ( #4761, #6917, #426, #1631 ) ) ;
#3226=EDGE_CURVE ( 'NONE', #4784, #2186, #2285, .T. ) ;
#3228=PLANE ( 'NONE',  #4079 ) ;
#3238=EDGE_LOOP ( 'NONE', ( #986, #7128, #1742, #7247 ) ) ;
#3251=DIRECTION ( 'NONE',  ( -1.000000000000000000, 0.000000000000000000, 0.000000000000000000 ) ) ;
#3253=CLOSED_SHELL ( 'NONE', ( #2504, #3857, #1157, #5287, #3739, #2459, #3912, #3294, #4144, #7082, #4341, #4098, #5509 ) ) ;
#3273=DIRECTION ( 'NONE',  ( 0.000000000000000000, 0.000000000000000000, 1.000000000000000000 ) ) ;
#3294=ADVANCED_FACE ( 'NONE', ( #7484 ), #5605, .F. ) ;
#3302=CIRCLE ( 'NONE', #6377, 12.50000000000000000 ) ;
#3308=FACE_OUTER_BOUND ( 'NONE', #4356, .T. ) ;
#3351=VERTEX_POINT ( 'NONE', #1232 ) ;
#3356=VERTEX_POINT ( 'NONE', #2590 ) ;
#3424=EDGE_CURVE ( 'NONE', #5200, #7492, #3836, .T. ) ;
#3443=CARTESIAN_POINT ( 'NONE',  ( 0.000000000000000000, 0.000000000000000000, 0.000000000000000000 ) ) ;
#3468=CARTESIAN_POINT ( 'NONE',  ( 75.00000000000000000, 10.56842436860067735, 0.000000000000000000 ) ) ;
#3485=VERTEX_POINT ( 'NONE', #4059 ) ;
#3517=EDGE_CURVE ( 'NONE', #3564, #2186, #6587, .T. ) ;
#3525=AXIS2_PLACEMENT_3D ( 'NONE', #1049, #2821, #7708 ) ;
#3564=VERTEX_POINT ( 'NONE', #1210 ) ;
#3583=AXIS2_PLACEMENT_3D ( 'NONE', #5942, #2946, #2903 ) ;
#3608=EDGE_CURVE ( 'NONE', #4076, #6800, #1992, .T. ) ;
#3639=AXIS2_PLACEMENT_3D ( 'NONE', #585, #3035, #3674 ) ;
#3640=DIRECTION ( 'NONE',  ( 0.4585571717133497538, 0.8886649088774990490, -0.000000000000000000 ) ) ;
#3649=DIRECTION ( 'NONE',  ( -1.000000000000000000, 0.000000000000000000, 0.000000000000000000 ) ) ;
#3650=AXIS2_PLACEMENT_3D ( 'NONE', #5858, #5250, #1527 ) ;
#3674=DIRECTION ( 'NONE',  ( -1.000000000000000000, 0.000000000000000000, 0.000000000000000000 ) ) ;
#3678=( NAMED_UNIT ( * ) PLANE_ANGLE_UNIT ( ) SI_UNIT ( $, .RADIAN. ) );
#3700=VECTOR ( 'NONE', #200, 1000.000000000000000 ) ;
#3739=ADVANCED_FACE ( 'NONE', ( #673, #7337, #4841 ), #2711, .F. ) ;
#3755=EDGE_CURVE ( 'NONE', #3564, #7759, #2518, .T. ) ;
#3763=CARTESIAN_POINT ( 'NONE',  ( 75.00000000000000000, 10.56842436860067735, 25.00000000000000000 ) ) ;
#3799=MECHANICAL_DESIGN_GEOMETRIC_PRESENTATION_REPRESENTATION('',(#1358),#7773);
#3825=EDGE_CURVE ( 'NONE', #4302, #1554, #1478, .T. ) ;
#3836=LINE ( 'NONE', #3468, #3028 ) ;
#3851=CARTESIAN_POINT ( 'NONE',  ( 0.000000000000000000, 0.000000000000000000, 0.000000000000000000 ) ) ;
#3857=ADVANCED_FACE ( 'NONE', ( #3877 ), #5074, .F. ) ;
#3877=FACE_OUTER_BOUND ( 'NONE', #399, .T. ) ;
#3892=EDGE_CURVE ( 'NONE', #7913, #957, #5588, .T. ) ;
#3905=ORIENTED_EDGE ( 'NONE', *, *, #7525, .F. ) ;
#3912=ADVANCED_FACE ( 'NONE', ( #6532 ), #2280, .F. ) ;
#3954=CARTESIAN_POINT ( 'NONE',  ( -8.959197987552832032, 23.33951095074251114, 0.000000000000000000 ) ) ;
#3965=DIRECTION ( 'NONE',  ( 0.000000000000000000, 0.000000000000000000, 1.000000000000000000 ) ) ;
#3972=ORIENTED_EDGE ( 'NONE', *, *, #1263, .F. ) ;
#4002=EDGE_LOOP ( 'NONE', ( #4795, #3972, #2688, #6659, #759, #6643, #120 ) ) ;
#4005=CARTESIAN_POINT ( 'NONE',  ( 162.5000000000000000, 1.990051048614448997E-14, 25.00000000000000000 ) ) ;
#4019=DIRECTION ( 'NONE',  ( 0.9335804380297001437, 0.3583679195021130526, 0.000000000000000000 ) ) ;
#4047=DIRECTION ( 'NONE',  ( -0.000000000000000000, -0.000000000000000000, -1.000000000000000000 ) ) ;
#4059=CARTESIAN_POINT ( 'NONE',  ( -12.50000000000000000, 0.000000000000000000, 25.00000000000000000 ) ) ;
#4067=EDGE_LOOP ( 'NONE', ( #197, #1946, #6181, #1484 ) ) ;
#4076=VERTEX_POINT ( 'NONE', #1148 ) ;
#4079=AXIS2_PLACEMENT_3D ( 'NONE', #1537, #6953, #6311 ) ;
#4086=ORIENTED_EDGE ( 'NONE', *, *, #4386, .T. ) ;
#4098=ADVANCED_FACE ( 'NONE', ( #4188 ), #7810, .F. ) ;
#4103=CARTESIAN_POINT ( 'NONE',  ( 0.000000000000000000, 0.000000000000000000, 25.00000000000000000 ) ) ;
#4110=CARTESIAN_POINT ( 'NONE',  ( 0.000000000000000000, 0.000000000000000000, 0.000000000000000000 ) ) ;
#4135=MANIFOLD_SOLID_BREP ( 'Yükseklik-Ekstrüzyon1', #3253 ) ;
#4144=ADVANCED_FACE ( 'NONE', ( #1417 ), #139, .T. ) ;
#4186=DIRECTION ( 'NONE',  ( 0.000000000000000000, 0.000000000000000000, 1.000000000000000000 ) ) ;
#4187=ORIENTED_EDGE ( 'NONE', *, *, #3517, .F. ) ;
#4188=FACE_OUTER_BOUND ( 'NONE', #7451, .T. ) ;
#4220=SHAPE_DEFINITION_REPRESENTATION ( #2710, #949 ) ;
#4247=ORIENTED_EDGE ( 'NONE', *, *, #1890, .F. ) ;
#4260=VECTOR ( 'NONE', #3140, 1000.000000000000227 ) ;
#4302=VERTEX_POINT ( 'NONE', #895 ) ;
#4341=ADVANCED_FACE ( 'NONE', ( #3308 ), #2097, .F. ) ;
#4348=CARTESIAN_POINT ( 'NONE',  ( 162.5000000000000000, 1.990051048614448997E-14, 0.000000000000000000 ) ) ;
#4356=EDGE_LOOP ( 'NONE', ( #2800, #5977, #2633, #4529 ) ) ;
#4360=EDGE_LOOP ( 'NONE', ( #6370, #2103, #296, #1416 ) ) ;
#4362=ORIENTED_EDGE ( 'NONE', *, *, #3755, .T. ) ;
#4366=CARTESIAN_POINT ( 'NONE',  ( 0.000000000000000000, 0.000000000000000000, 0.000000000000000000 ) ) ;
#4379=DIRECTION ( 'NONE',  ( -0.000000000000000000, -0.000000000000000000, -1.000000000000000000 ) ) ;
#4386=EDGE_CURVE ( 'NONE', #957, #7913, #5075, .T. ) ;
#4461=CIRCLE ( 'NONE', #3583, 12.50000000000000000 ) ;
#4513=DIRECTION ( 'NONE',  ( 0.000000000000000000, 0.000000000000000000, 1.000000000000000000 ) ) ;
#4529=ORIENTED_EDGE ( 'NONE', *, *, #3517, .T. ) ;
#4543=CARTESIAN_POINT ( 'NONE',  ( 138.5360707071662887, -22.21662272193747256, 25.00000000000000000 ) ) ;
#4556=AXIS2_PLACEMENT_3D ( 'NONE', #2432, #4751, #1227 ) ;
#4594=DIRECTION ( 'NONE',  ( -0.4585571717133501424, 0.8886649088774988270, 0.000000000000000000 ) ) ;
#4601=VERTEX_POINT ( 'NONE', #2777 ) ;
#4633=LINE ( 'NONE', #5116, #702 ) ;
#4650=AXIS2_PLACEMENT_3D ( 'NONE', #3443, #5888, #392 ) ;
#4656=EDGE_LOOP ( 'NONE', ( #2330, #5802, #4783, #4247 ) ) ;
#4720=PRODUCT_DEFINITION ( 'UNKNOWN', '', #5128, #7282 ) ;
#4751=DIRECTION ( 'NONE',  ( -0.000000000000000000, -0.000000000000000000, -1.000000000000000000 ) ) ;
#4755=DIRECTION ( 'NONE',  ( -0.9335804380297003657, 0.3583679195021128305, 0.000000000000000000 ) ) ;
#4759=ORIENTED_EDGE ( 'NONE', *, *, #5069, .T. ) ;
#4761=ORIENTED_EDGE ( 'NONE', *, *, #1061, .F. ) ;
#4783=ORIENTED_EDGE ( 'NONE', *, *, #1911, .T. ) ;
#4784=VERTEX_POINT ( 'NONE', #6104 ) ;
#4788=CIRCLE ( 'NONE', #5564, 24.99999999999999289 ) ;
#4795=ORIENTED_EDGE ( 'NONE', *, *, #6400, .F. ) ;
#4808=CARTESIAN_POINT ( 'NONE',  ( 75.00000000000000000, 10.56842436860067735, 25.00000000000000000 ) ) ;
#4821=DIRECTION ( 'NONE',  ( -1.000000000000000000, 0.000000000000000000, 0.000000000000000000 ) ) ;
#4841=FACE_BOUND ( 'NONE', #313, .T. ) ;
#4873=EDGE_CURVE ( 'NONE', #886, #7894, #7858, .T. ) ;
#4902=ORIENTED_EDGE ( 'NONE', *, *, #5241, .T. ) ;
#4913=ORIENTED_EDGE ( 'NONE', *, *, #6302, .F. ) ;
#4934=DIRECTION ( 'NONE',  ( -1.000000000000000000, 0.000000000000000000, 0.000000000000000000 ) ) ;
#4945=SHAPE_REPRESENTATION_RELATIONSHIP ( 'NONE' , 'NONE' ,  #949, #1434 ) ;
#4947=CARTESIAN_POINT ( 'NONE',  ( 150.0000000000000000, 1.836970198721029747E-14, 25.00000000000000000 ) ) ;
#4951=CARTESIAN_POINT ( 'NONE',  ( 12.50000000000000000, 1.530808498934191521E-15, 25.00000000000000000 ) ) ;
#4976=CARTESIAN_POINT ( 'NONE',  ( 0.000000000000000000, 0.000000000000000000, 25.00000000000000000 ) ) ;
#4997=VERTEX_POINT ( 'NONE', #3063 ) ;
#5069=EDGE_CURVE ( 'NONE', #6800, #4076, #3302, .T. ) ;
#5074=CYLINDRICAL_SURFACE ( 'NONE', #1098, 12.50000000000000000 ) ;
#5075=CIRCLE ( 'NONE', #2654, 12.50000000000001066 ) ;
#5116=CARTESIAN_POINT ( 'NONE',  ( -25.00000000000000711, 0.000000000000000000, 25.00000000000000000 ) ) ;
#5120=DIRECTION ( 'NONE',  ( -0.9335804380297003657, 0.3583679195021128305, 0.000000000000000000 ) ) ;
#5128=PRODUCT_DEFINITION_FORMATION_WITH_SPECIFIED_SOURCE ( 'ANY', '', #2198, .NOT_KNOWN. ) ;
#5131=CARTESIAN_POINT ( 'NONE',  ( 137.4999999999999716, 1.836970198721029747E-14, 25.00000000000000000 ) ) ;
#5197=CARTESIAN_POINT ( 'NONE',  ( 75.00000000000000000, 10.56842436860067735, 0.000000000000000000 ) ) ;
#5200=VERTEX_POINT ( 'NONE', #6904 ) ;
#5219=ORIENTED_EDGE ( 'NONE', *, *, #6253, .T. ) ;
#5241=EDGE_CURVE ( 'NONE', #3351, #4784, #6045, .T. ) ;
#5250=DIRECTION ( 'NONE',  ( -0.000000000000000000, -0.000000000000000000, -1.000000000000000000 ) ) ;
#5287=ADVANCED_FACE ( 'NONE', ( #5480, #5898, #3000 ), #6810, .T. ) ;
#5313=ORIENTED_EDGE ( 'NONE', *, *, #3892, .F. ) ;
#5340=CARTESIAN_POINT ( 'NONE',  ( -12.50000000000000000, 0.000000000000000000, 25.00000000000000000 ) ) ;
#5378=ORIENTED_EDGE ( 'NONE', *, *, #3608, .T. ) ;
#5427=CARTESIAN_POINT ( 'NONE',  ( 150.0000000000000000, 1.836970198721029747E-14, 25.00000000000000000 ) ) ;
#5437=DIRECTION ( 'NONE',  ( 0.000000000000000000, 0.000000000000000000, 1.000000000000000000 ) ) ;
#5480=FACE_BOUND ( 'NONE', #5814, .T. ) ;
#5498=VECTOR ( 'NONE', #2215, 1000.000000000000000 ) ;
#5504=CARTESIAN_POINT ( 'NONE',  ( 0.000000000000000000, 0.000000000000000000, 25.00000000000000000 ) ) ;
#5509=ADVANCED_FACE ( 'NONE', ( #3156 ), #98, .F. ) ;
#5515=( NAMED_UNIT ( * ) SI_UNIT ( $, .STERADIAN. ) SOLID_ANGLE_UNIT ( ) );
#5537=AXIS2_PLACEMENT_3D ( 'NONE', #5504, #1843, #4934 ) ;
#5564=AXIS2_PLACEMENT_3D ( 'NONE', #1683, #7785, #3649 ) ;
#5568=DIRECTION ( 'NONE',  ( 0.000000000000000000, 0.000000000000000000, 1.000000000000000000 ) ) ;
#5588=CIRCLE ( 'NONE', #7883, 12.50000000000001066 ) ;
#5605=PLANE ( 'NONE',  #6732 ) ;
#5651=CARTESIAN_POINT ( 'NONE',  ( 0.000000000000000000, 0.000000000000000000, 25.00000000000000000 ) ) ;
#5665=EDGE_CURVE ( 'NONE', #4997, #2860, #7594, .T. ) ;
#5704=CYLINDRICAL_SURFACE ( 'NONE', #7233, 25.00000000000000711 ) ;
#5715=FACE_OUTER_BOUND ( 'NONE', #1096, .T. ) ;
#5723=DIRECTION ( 'NONE',  ( 1.000000000000000000, 0.000000000000000000, 0.000000000000000000 ) ) ;
#5725=EDGE_CURVE ( 'NONE', #3485, #4601, #235, .T. ) ;
#5742=AXIS2_PLACEMENT_3D ( 'NONE', #1149, #5437, #6454 ) ;
#5764=ORIENTED_EDGE ( 'NONE', *, *, #3825, .T. ) ;
#5785=AXIS2_PLACEMENT_3D ( 'NONE', #4110, #4186, #2351 ) ;
#5802=ORIENTED_EDGE ( 'NONE', *, *, #3892, .T. ) ;
#5814=EDGE_LOOP ( 'NONE', ( #6689, #4913 ) ) ;
#5858=CARTESIAN_POINT ( 'NONE',  ( 150.0000000000000000, 1.836970198721029747E-14, 25.00000000000000000 ) ) ;
#5886=ORIENTED_EDGE ( 'NONE', *, *, #1654, .T. ) ;
#5888=DIRECTION ( 'NONE',  ( 0.000000000000000000, 0.000000000000000000, 1.000000000000000000 ) ) ;
#5898=FACE_OUTER_BOUND ( 'NONE', #6349, .T. ) ;
#5930=CARTESIAN_POINT ( 'NONE',  ( -8.959197987552832032, 23.33951095074251114, 25.00000000000000000 ) ) ;
#5942=CARTESIAN_POINT ( 'NONE',  ( 0.000000000000000000, 0.000000000000000000, 25.00000000000000000 ) ) ;
#5952=ORIENTED_EDGE ( 'NONE', *, *, #3825, .F. ) ;
#5971=CARTESIAN_POINT ( 'NONE',  ( 158.9591979875528409, 23.33951095074252891, 0.000000000000000000 ) ) ;
#5977=ORIENTED_EDGE ( 'NONE', *, *, #1589, .F. ) ;
#6033=APPLICATION_CONTEXT ( 'automotive_design' ) ;
#6045=LINE ( 'NONE', #7738, #2536 ) ;
#6058=ORIENTED_EDGE ( 'NONE', *, *, #3226, .T. ) ;
#6070=VECTOR ( 'NONE', #693, 1000.000000000000000 ) ;
#6082=( NAMED_UNIT ( * ) SI_UNIT ( $, .STERADIAN. ) SOLID_ANGLE_UNIT ( ) );
#6101=AXIS2_PLACEMENT_3D ( 'NONE', #2638, #151, #1947 ) ;
#6104=CARTESIAN_POINT ( 'NONE',  ( 158.9591979875528409, 23.33951095074252891, 0.000000000000000000 ) ) ;
#6107=CARTESIAN_POINT ( 'NONE',  ( 75.00000000000000000, 55.56842436860067380, 0.000000000000000000 ) ) ;
#6146=DIRECTION ( 'NONE',  ( 0.000000000000000000, 0.000000000000000000, 1.000000000000000000 ) ) ;
#6147=CYLINDRICAL_SURFACE ( 'NONE', #5537, 25.00000000000000711 ) ;
#6177=EDGE_CURVE ( 'NONE', #7492, #2860, #2373, .T. ) ;
#6181=ORIENTED_EDGE ( 'NONE', *, *, #6207, .F. ) ;
#6207=EDGE_CURVE ( 'NONE', #7894, #4997, #368, .T. ) ;
#6242=DIRECTION ( 'NONE',  ( -0.8886649088774989380, 0.4585571717133496983, 0.000000000000000000 ) ) ;
#6253=EDGE_CURVE ( 'NONE', #3485, #4076, #7707, .T. ) ;
#6302=EDGE_CURVE ( 'NONE', #4601, #3485, #4461, .T. ) ;
#6311=DIRECTION ( 'NONE',  ( 0.9335804380297003657, -0.3583679195021128305, 0.000000000000000000 ) ) ;
#6318=CARTESIAN_POINT ( 'NONE',  ( 0.000000000000000000, 0.000000000000000000, 25.00000000000000000 ) ) ;
#6349=EDGE_LOOP ( 'NONE', ( #5886, #7027, #1503, #2096, #7675, #7681, #4362 ) ) ;
#6351=AXIS2_PLACEMENT_3D ( 'NONE', #3052, #5568, #2443 ) ;
#6364=DIRECTION ( 'NONE',  ( -1.000000000000000000, 0.000000000000000000, 0.000000000000000000 ) ) ;
#6370=ORIENTED_EDGE ( 'NONE', *, *, #2673, .T. ) ;
#6377=AXIS2_PLACEMENT_3D ( 'NONE', #3851, #796, #723 ) ;
#6392=CIRCLE ( 'NONE', #2426, 25.00000000000000711 ) ;
#6400=EDGE_CURVE ( 'NONE', #7887, #2392, #6392, .T. ) ;
#6454=DIRECTION ( 'NONE',  ( 1.000000000000000000, 0.000000000000000000, -0.000000000000000000 ) ) ;
#6484=CARTESIAN_POINT ( 'NONE',  ( 162.5000000000000000, 1.990051048614448997E-14, 25.00000000000000000 ) ) ;
#6532=FACE_OUTER_BOUND ( 'NONE', #3238, .T. ) ;
#6553=EDGE_CURVE ( 'NONE', #7894, #7492, #6865, .T. ) ;
#6582=DIRECTION ( 'NONE',  ( 0.8886649088774989380, -0.4585571717133497538, 0.000000000000000000 ) ) ;
#6587=LINE ( 'NONE', #1092, #6984 ) ;
#6604=EDGE_CURVE ( 'NONE', #7913, #1554, #2208, .T. ) ;
#6633=CARTESIAN_POINT ( 'NONE',  ( 150.0000000000000000, 1.836970198721029747E-14, 25.00000000000000000 ) ) ;
#6634=DIRECTION ( 'NONE',  ( 1.000000000000000000, 0.000000000000000000, 0.000000000000000000 ) ) ;
#6643=ORIENTED_EDGE ( 'NONE', *, *, #3424, .F. ) ;
#6659=ORIENTED_EDGE ( 'NONE', *, *, #2673, .F. ) ;
#6689=ORIENTED_EDGE ( 'NONE', *, *, #5725, .F. ) ;
#6720=VECTOR ( 'NONE', #3158, 1000.000000000000000 ) ;
#6732=AXIS2_PLACEMENT_3D ( 'NONE', #3763, #3640, #6242 ) ;
#6781=VECTOR ( 'NONE', #2820, 1000.000000000000227 ) ;
#6800=VERTEX_POINT ( 'NONE', #7891 ) ;
#6804=LINE ( 'NONE', #1381, #6720 ) ;
#6810=PLANE ( 'NONE',  #5742 ) ;
#6836=DIRECTION ( 'NONE',  ( -1.000000000000000000, 0.000000000000000000, 0.000000000000000000 ) ) ;
#6865=LINE ( 'NONE', #1363, #3700 ) ;
#6896=AXIS2_PLACEMENT_3D ( 'NONE', #2550, #4379, #741 ) ;
#6904=CARTESIAN_POINT ( 'NONE',  ( 11.46392929283375928, -22.21662272193747256, 0.000000000000000000 ) ) ;
#6917=ORIENTED_EDGE ( 'NONE', *, *, #3057, .T. ) ;
#6950=LINE ( 'NONE', #2052, #6070 ) ;
#6953=DIRECTION ( 'NONE',  ( -0.3583679195021128305, -0.9335804380297003657, 0.000000000000000000 ) ) ;
#6970=DIRECTION ( 'NONE',  ( -0.000000000000000000, -0.000000000000000000, -1.000000000000000000 ) ) ;
#6981=CIRCLE ( 'NONE', #3525, 25.00000000000000711 ) ;
#6984=VECTOR ( 'NONE', #2986, 1000.000000000000000 ) ;
#6998=DIRECTION ( 'NONE',  ( -0.000000000000000000, -0.000000000000000000, -1.000000000000000000 ) ) ;
#7016=CARTESIAN_POINT ( 'NONE',  ( 158.9591979875528409, 23.33951095074252891, 25.00000000000000000 ) ) ;
#7027=ORIENTED_EDGE ( 'NONE', *, *, #1061, .T. ) ;
#7082=ADVANCED_FACE ( 'NONE', ( #5715 ), #3228, .F. ) ;
#7083=CARTESIAN_POINT ( 'NONE',  ( 75.00000000000000000, 10.56842436860067735, 25.00000000000000000 ) ) ;
#7100=FACE_OUTER_BOUND ( 'NONE', #2943, .T. ) ;
#7110=CARTESIAN_POINT ( 'NONE',  ( 75.00000000000000000, 10.56842436860067735, 0.000000000000000000 ) ) ;
#7125=VECTOR ( 'NONE', #2068, 1000.000000000000227 ) ;
#7128=ORIENTED_EDGE ( 'NONE', *, *, #6553, .F. ) ;
#7177=ORIENTED_EDGE ( 'NONE', *, *, #4386, .F. ) ;
#7186=DIRECTION ( 'NONE',  ( -0.000000000000000000, -0.000000000000000000, -1.000000000000000000 ) ) ;
#7198=ORIENTED_EDGE ( 'NONE', *, *, #5725, .T. ) ;
#7233=AXIS2_PLACEMENT_3D ( 'NONE', #4976, #7466, #3251 ) ;
#7247=ORIENTED_EDGE ( 'NONE', *, *, #911, .T. ) ;
#7252=( LENGTH_UNIT ( ) NAMED_UNIT ( * ) SI_UNIT ( .MILLI., .METRE. ) );
#7282=PRODUCT_DEFINITION_CONTEXT ( 'detailed design', #6033, 'design' ) ;
#7294=VECTOR ( 'NONE', #5120, 1000.000000000000114 ) ;
#7337=FACE_BOUND ( 'NONE', #7683, .T. ) ;
#7373=VECTOR ( 'NONE', #4755, 1000.000000000000114 ) ;
#7405=DIRECTION ( 'NONE',  ( -0.000000000000000000, -0.000000000000000000, -1.000000000000000000 ) ) ;
#7428=DIRECTION ( 'NONE',  ( 0.8886649088774987160, 0.4585571717133501424, -0.000000000000000000 ) ) ;
#7429=DIRECTION ( 'NONE',  ( 1.000000000000000000, 0.000000000000000000, 0.000000000000000000 ) ) ;
#7451=EDGE_LOOP ( 'NONE', ( #1223, #3164, #5219, #3017 ) ) ;
#7466=DIRECTION ( 'NONE',  ( -0.000000000000000000, -0.000000000000000000, -1.000000000000000000 ) ) ;
#7484=FACE_OUTER_BOUND ( 'NONE', #4067, .T. ) ;
#7492=VERTEX_POINT ( 'NONE', #5197 ) ;
#7513=AXIS2_PLACEMENT_3D ( 'NONE', #2139, #1617, #4019 ) ;
#7525=EDGE_CURVE ( 'NONE', #3351, #3564, #2201, .T. ) ;
#7551=CARTESIAN_POINT ( 'NONE',  ( 11.46392929283375928, -22.21662272193747256, 25.00000000000000000 ) ) ;
#7567=CARTESIAN_POINT ( 'NONE',  ( 150.0000000000000000, 1.836970198721029747E-14, 25.00000000000000000 ) ) ;
#7594=LINE ( 'NONE', #4543, #106 ) ;
#7610=CIRCLE ( 'NONE', #57, 25.00000000000000711 ) ;
#7675=ORIENTED_EDGE ( 'NONE', *, *, #1888, .T. ) ;
#7681=ORIENTED_EDGE ( 'NONE', *, *, #7525, .T. ) ;
#7683=EDGE_LOOP ( 'NONE', ( #5378, #4759 ) ) ;
#7707=LINE ( 'NONE', #5340, #5498 ) ;
#7708=DIRECTION ( 'NONE',  ( 1.000000000000000000, 0.000000000000000000, 0.000000000000000000 ) ) ;
#7738=CARTESIAN_POINT ( 'NONE',  ( 158.9591979875528409, 23.33951095074252891, 25.00000000000000000 ) ) ;
#7759=VERTEX_POINT ( 'NONE', #5930 ) ;
#7761=DIRECTION ( 'NONE',  ( 0.000000000000000000, 0.000000000000000000, 1.000000000000000000 ) ) ;
#7773=( GEOMETRIC_REPRESENTATION_CONTEXT ( 3 ) GLOBAL_UNCERTAINTY_ASSIGNED_CONTEXT ( ( #2712 ) ) GLOBAL_UNIT_ASSIGNED_CONTEXT ( ( #7252, #551, #6082 ) ) REPRESENTATION_CONTEXT ( 'NONE', 'WORKASPACE' ) );
#7785=DIRECTION ( 'NONE',  ( 0.000000000000000000, 0.000000000000000000, 1.000000000000000000 ) ) ;
#7810=CYLINDRICAL_SURFACE ( 'NONE', #4556, 12.50000000000000000 ) ;
#7858=LINE ( 'NONE', #4808, #3049 ) ;
#7870=DIRECTION ( 'NONE',  ( 0.000000000000000000, 0.000000000000000000, 1.000000000000000000 ) ) ;
#7883=AXIS2_PLACEMENT_3D ( 'NONE', #7567, #4513, #6364 ) ;
#7887=VERTEX_POINT ( 'NONE', #3954 ) ;
#7891=CARTESIAN_POINT ( 'NONE',  ( 12.50000000000000000, 1.530808498934191521E-15, 0.000000000000000000 ) ) ;
#7894=VERTEX_POINT ( 'NONE', #7083 ) ;
#7913=VERTEX_POINT ( 'NONE', #6484 ) ;
#7942=COLOUR_RGB('Light Blue',0.38,0.62,0.78);
#7943=FILL_AREA_STYLE_COLOUR('',#7942);
#7944=FILL_AREA_STYLE('',(#7943));
#7945=SURFACE_STYLE_FILL_AREA(#7944);
#7946=SURFACE_SIDE_STYLE('',(#7945));
#7947=SURFACE_STYLE_USAGE(.BOTH.,#7946);
#7948=PRESENTATION_STYLE_ASSIGNMENT((#7947));
ENDSEC;
END-ISO-10303-21;
